ISO-10303-21;
HEADER;
FILE_DESCRIPTION (('STEP AP214'),
    '1' );
FILE_NAME ( 'M6 Thin Hex Nut.step', '2026-10-06T08:24:41', ( '' ), ( '' ), 'STEP AP214', 'Unspecified', '' );
FILE_SCHEMA (( 'AUTOMOTIVE_DESIGN' ));
ENDSEC;
DATA;
#15=EDGE_LOOP ( 'NONE', ( #27467, #1263, #14618, #2315 ) ) ;
#31=( BOUNDED_CURVE ( )  B_SPLINE_CURVE ( 2, ( #4927, #4785, #24416 ),
 .UNSPECIFIED., .F., .T. ) 
 B_SPLINE_CURVE_WITH_KNOTS ( ( 3, 3 ),
 ( 0.000000000000000000, 0.5842180690389588982 ),
 .UNSPECIFIED. ) 
 CURVE ( )  GEOMETRIC_REPRESENTATION_ITEM ( )  RATIONAL_B_SPLINE_CURVE ( ( 1.000000000000000000, 1.154700538379253905, 1.000000000000000000 ) ) 
 REPRESENTATION_ITEM ( '' )  ) ;
#73=AXIS2_PLACEMENT_3D ( 'NONE', #23725, #21593, #23590 ) ;
#93=SURFACE_STYLE_USAGE ( .BOTH. , #2166 ) ;
#97=LINE ( 'NONE', #15591, #22935 ) ;
#149=DIRECTION ( 'NONE',  ( 1.000000000000000000, 0.000000000000000000, 0.000000000000000000 ) ) ;
#163=PRODUCT ( 'M6 Thin Hex Nut', 'M6 Thin Hex Nut', '', ( #11511 ) ) ;
#183=CARTESIAN_POINT ( 'NONE',  ( 0.1259842519685039353, 0.1751968503937007815, 0.000000000000000000 ) ) ;
#224=( CONVERSION_BASED_UNIT ( 'INCH', #8931 ) LENGTH_UNIT ( ) NAMED_UNIT ( #18982 ) ) ;
#227=AXIS2_PLACEMENT_3D ( 'NONE', #3508, #14722, #27552 ) ;
#229=CARTESIAN_POINT ( 'NONE',  ( 0.03008364706454716778, 0.1136516277932332619, 0.1968503937007874127 ) ) ;
#244=CIRCLE ( 'NONE', #20043, 0.1751968503937007815 ) ;
#302=AXIS2_PLACEMENT_3D ( 'NONE', #2958, #11178, #15703 ) ;
#352=FILL_AREA_STYLE_COLOUR ( '', #20221 ) ;
#368=ORIENTED_EDGE ( 'NONE', *, *, #7108, .F. ) ;
#388=DIRECTION ( 'NONE',  ( 0.000000000000000000, 0.000000000000000000, -1.000000000000000000 ) ) ;
#560=ORIENTED_EDGE ( 'NONE', *, *, #19691, .F. ) ;
#633=AXIS2_PLACEMENT_3D ( 'NONE', #14574, #25279, #27129 ) ;
#657=VERTEX_POINT ( 'NONE', #15970 ) ;
#673=ADVANCED_FACE ( 'NONE', ( #14428 ), #18626, .T. ) ;
#721=CARTESIAN_POINT ( 'NONE',  ( 0.006151574803149606648, 0.000000000000000000, 0.000000000000000000 ) ) ;
#722=VECTOR ( 'NONE', #23360, 39.37007874015748854 ) ;
#737=ADVANCED_FACE ( 'NONE', ( #1144 ), #9744, .T. ) ;
#790=FACE_OUTER_BOUND ( 'NONE', #25634, .T. ) ;
#970=AXIS2_PLACEMENT_3D ( 'NONE', #18823, #8110, #11923 ) ;
#1093=PLANE ( 'NONE',  #21809 ) ;
#1106=ORIENTED_EDGE ( 'NONE', *, *, #4796, .T. ) ;
#1128=DIRECTION ( 'NONE',  ( 1.000000000000000000, 0.000000000000000000, 0.000000000000000000 ) ) ;
#1144=FACE_OUTER_BOUND ( 'NONE', #12935, .T. ) ;
#1228=EDGE_CURVE ( 'NONE', #3526, #26154, #15140, .T. ) ;
#1263=ORIENTED_EDGE ( 'NONE', *, *, #3666, .T. ) ;
#1329=DIRECTION ( 'NONE',  ( 1.000000000000000000, 0.000000000000000000, 0.000000000000000000 ) ) ;
#1367=DIRECTION ( 'NONE',  ( 1.000000000000000000, 0.000000000000000000, 0.000000000000000000 ) ) ;
#1448=EDGE_LOOP ( 'NONE', ( #11858, #8037, #16293, #11555 ) ) ;
#1466=ADVANCED_FACE ( 'NONE', ( #790 ), #23242, .F. ) ;
#1505=DIRECTION ( 'NONE',  ( -1.000000000000000000, 0.000000000000000000, 0.000000000000000000 ) ) ;
#1507=FACE_OUTER_BOUND ( 'NONE', #3850, .T. ) ;
#1513=CIRCLE ( 'NONE', #14167, 0.1751968503937007815 ) ;
#1597=ORIENTED_EDGE ( 'NONE', *, *, #23655, .F. ) ;
#1653=DIRECTION ( 'NONE',  ( 0.000000000000000000, 0.000000000000000000, -1.000000000000000000 ) ) ;
#1689=CARTESIAN_POINT ( 'NONE',  ( 0.03008364706454716778, 0.1136516277932340530, -0.1968503937007874127 ) ) ;
#1748=ORIENTED_EDGE ( 'NONE', *, *, #22387, .F. ) ;
#1846=ORIENTED_EDGE ( 'NONE', *, *, #19267, .F. ) ;
#1849=ORIENTED_EDGE ( 'NONE', *, *, #8001, .T. ) ;
#1853=LINE ( 'NONE', #23488, #2325 ) ;
#1944=CARTESIAN_POINT ( 'NONE',  ( 0.006151574803149606648, -1.315836188112322458E-17, 0.1074461786882927178 ) ) ;
#1957=( BOUNDED_CURVE ( )  B_SPLINE_CURVE ( 2, ( #3595, #27346, #24646 ),
 .UNSPECIFIED., .F., .T. ) 
 B_SPLINE_CURVE_WITH_KNOTS ( ( 3, 3 ),
 ( 0.000000000000000000, 0.5842180690389598974 ),
 .UNSPECIFIED. ) 
 CURVE ( )  GEOMETRIC_REPRESENTATION_ITEM ( )  RATIONAL_B_SPLINE_CURVE ( ( 1.000000000000000000, 1.154700538379251906, 1.000000000000000000 ) ) 
 REPRESENTATION_ITEM ( '' )  ) ;
#2063=CARTESIAN_POINT ( 'NONE',  ( 0.006151574803149606648, 0.000000000000000000, 0.000000000000000000 ) ) ;
#2073=EDGE_CURVE ( 'NONE', #8851, #9496, #18343, .T. ) ;
#2117=ORIENTED_EDGE ( 'NONE', *, *, #24084, .F. ) ;
#2155=VERTEX_POINT ( 'NONE', #7889 ) ;
#2166=SURFACE_SIDE_STYLE ('',( #25102 ) ) ;
#2182=VECTOR ( 'NONE', #21944, 39.37007874015748143 ) ;
#2315=ORIENTED_EDGE ( 'NONE', *, *, #8864, .F. ) ;
#2325=VECTOR ( 'NONE', #23756, 39.37007874015748143 ) ;
#2348=ORIENTED_EDGE ( 'NONE', *, *, #24166, .F. ) ;
#2350=DIRECTION ( 'NONE',  ( 0.000000000000000000, 1.000000000000000000, 0.000000000000000000 ) ) ;
#2385=VECTOR ( 'NONE', #25591, 39.37007874015748854 ) ;
#2395=VECTOR ( 'NONE', #3087, 39.37007874015748854 ) ;
#2416=VECTOR ( 'NONE', #22375, 39.37007874015748854 ) ;
#2437=VERTEX_POINT ( 'NONE', #9082 ) ;
#2464=CARTESIAN_POINT ( 'NONE',  ( 0.03008364706454716778, 0.2273032555864669124, 0.000000000000000000 ) ) ;
#2564=EDGE_CURVE ( 'NONE', #3577, #11261, #6383, .T. ) ;
#2613=DIRECTION ( 'NONE',  ( 1.000000000000000000, 0.000000000000000000, 0.000000000000000000 ) ) ;
#2738=DIRECTION ( 'NONE',  ( -1.000000000000000000, 0.000000000000000000, 0.000000000000000000 ) ) ;
#2785=ORIENTED_EDGE ( 'NONE', *, *, #8151, .T. ) ;
#2827=( BOUNDED_CURVE ( )  B_SPLINE_CURVE ( 2, ( #16964, #14869, #4109 ),
 .UNSPECIFIED., .F., .T. ) 
 B_SPLINE_CURVE_WITH_KNOTS ( ( 3, 3 ),
 ( 0.000000000000000000, 0.5842180690389568998 ),
 .UNSPECIFIED. ) 
 CURVE ( )  GEOMETRIC_REPRESENTATION_ITEM ( )  RATIONAL_B_SPLINE_CURVE ( ( 1.000000000000000000, 1.154700538379249908, 1.000000000000000000 ) ) 
 REPRESENTATION_ITEM ( '' )  ) ;
#2958=CARTESIAN_POINT ( 'NONE',  ( -0.4895985792973480133, 0.000000000000000000, 0.000000000000000000 ) ) ;
#3023=ORIENTED_EDGE ( 'NONE', *, *, #2564, .T. ) ;
#3025=ORIENTED_EDGE ( 'NONE', *, *, #10718, .F. ) ;
#3032=ORIENTED_EDGE ( 'NONE', *, *, #24525, .T. ) ;
#3057=ORIENTED_EDGE ( 'NONE', *, *, #24084, .T. ) ;
#3058=MECHANICAL_DESIGN_GEOMETRIC_PRESENTATION_REPRESENTATION('',(#18409),#19323);
#3087=DIRECTION ( 'NONE',  ( 0.5000000010362839475, -1.060575237992202059E-16, -0.8660254031861397417 ) ) ;
#3145=LINE ( 'NONE', #27043, #2416 ) ;
#3237=CONICAL_SURFACE ( 'NONE', #23126, 0.2012500529900838608, 1.047197550000000144 ) ;
#3262=AXIS2_PLACEMENT_3D ( 'NONE', #6731, #2738, #388 ) ;
#3317=DIRECTION ( 'NONE',  ( -1.000000000000000000, 0.000000000000000000, 0.000000000000000000 ) ) ;
#3328=CARTESIAN_POINT ( 'NONE',  ( 0.03008364706454716778, 0.1136516277932340530, -0.1968503937007874127 ) ) ;
#3436=EDGE_LOOP ( 'NONE', ( #21121, #8303 ) ) ;
#3443=ORIENTED_EDGE ( 'NONE', *, *, #13804, .F. ) ;
#3447=MANIFOLD_SOLID_BREP ( 'M6 Thin Hex Nut', #10992 ) ;
#3508=CARTESIAN_POINT ( 'NONE',  ( 0.01230314960629921330, 0.000000000000000000, 0.000000000000000000 ) ) ;
#3526=VERTEX_POINT ( 'NONE', #12203 ) ;
#3577=VERTEX_POINT ( 'NONE', #14915 ) ;
#3594=PLANE ( 'NONE',  #4329 ) ;
#3595=CARTESIAN_POINT ( 'NONE',  ( 0.09590060490395689585, -0.1136516277932334562, 0.1968503937007874127 ) ) ;
#3611=DIRECTION ( 'NONE',  ( 0.000000000000000000, 1.000000000000000000, 0.000000000000000000 ) ) ;
#3635=ORIENTED_EDGE ( 'NONE', *, *, #16621, .F. ) ;
#3648=CARTESIAN_POINT ( 'NONE',  ( 0.1287090038540881498, 0.1704774416898497957, 0.09842519685039405331 ) ) ;
#3656=CARTESIAN_POINT ( 'NONE',  ( -0.002724751885583818600, 4.306736220472441732E-16, -0.1968503937007877458 ) ) ;
#3659=EDGE_CURVE ( 'NONE', #8851, #18698, #97, .T. ) ;
#3665=DIRECTION ( 'NONE',  ( 0.000000000000000000, 0.000000000000000000, 1.000000000000000000 ) ) ;
#3666=EDGE_CURVE ( 'NONE', #12544, #11206, #13316, .T. ) ;
#3784=( LENGTH_UNIT ( ) NAMED_UNIT ( * ) SI_UNIT ( $, .METRE. ) ) ;
#3807=AXIS2_PLACEMENT_3D ( 'NONE', #7636, #3812, #12142 ) ;
#3812=DIRECTION ( 'NONE',  ( 0.000000000000000000, 0.8660254037844388186, -0.4999999999999998890 ) ) ;
#3844=VERTEX_POINT ( 'NONE', #3328 ) ;
#3850=EDGE_LOOP ( 'NONE', ( #3032, #12389 ) ) ;
#3933=ORIENTED_EDGE ( 'NONE', *, *, #16910, .F. ) ;
#4027=CARTESIAN_POINT ( 'NONE',  ( 0.03008364706454716778, 0.1136516277932334562, 0.1968503937007874127 ) ) ;
#4105=DIRECTION ( 'NONE',  ( 0.000000000000000000, 0.000000000000000000, 1.000000000000000000 ) ) ;
#4109=CARTESIAN_POINT ( 'NONE',  ( 0.09590060490395689585, -0.1136516277932324709, -0.1968503937007874127 ) ) ;
#4329=AXIS2_PLACEMENT_3D ( 'NONE', #23258, #12223, #12644 ) ;
#4355=ORIENTED_EDGE ( 'NONE', *, *, #1228, .T. ) ;
#4434=CARTESIAN_POINT ( 'NONE',  ( 0.03008364706454716778, -0.1136516277932334562, 0.1968503937007874127 ) ) ;
#4489=CARTESIAN_POINT ( 'NONE',  ( 0.01504182353227358389, 0.000000000000000000, 0.000000000000000000 ) ) ;
#4546=DIRECTION ( 'NONE',  ( 0.000000000000000000, 0.000000000000000000, -1.000000000000000000 ) ) ;
#4600=VECTOR ( 'NONE', #27809, 39.37007874015748854 ) ;
#4746=EDGE_LOOP ( 'NONE', ( #8223, #13844, #16495, #15110 ) ) ;
#4785=CARTESIAN_POINT ( 'NONE',  ( 0.1287090038540879555, -0.1704774416898497957, 0.09842519685039353983 ) ) ;
#4796=EDGE_CURVE ( 'NONE', #19119, #20886, #12731, .T. ) ;
#4927=CARTESIAN_POINT ( 'NONE',  ( 0.09590060490395689585, -0.2273032555864669124, 2.185478346456692557E-17 ) ) ;
#5013=ORIENTED_EDGE ( 'NONE', *, *, #24359, .T. ) ;
#5031=CARTESIAN_POINT ( 'NONE',  ( 0.000000000000000000, -0.2273032555864669124, 3.963736220472441631E-17 ) ) ;
#5219=DIRECTION ( 'NONE',  ( 1.000000000000000000, 0.000000000000000000, 0.000000000000000000 ) ) ;
#5229=CARTESIAN_POINT ( 'NONE',  ( 0.000000000000000000, 0.000000000000000000, 0.000000000000000000 ) ) ;
#5261=ADVANCED_FACE ( 'NONE', ( #8063 ), #20627, .T. ) ;
#5317=EDGE_CURVE ( 'NONE', #9496, #3844, #5760, .T. ) ;
#5375=DIRECTION ( 'NONE',  ( 0.000000000000000000, 0.000000000000000000, 1.000000000000000000 ) ) ;
#5396=CARTESIAN_POINT ( 'NONE',  ( 0.09590060490395689585, -0.1136516277932324709, -0.1968503937007874127 ) ) ;
#5400=VECTOR ( 'NONE', #9652, 39.37007874015748143 ) ;
#5414=ORIENTED_EDGE ( 'NONE', *, *, #27515, .F. ) ;
#5647=DIRECTION ( 'NONE',  ( 1.000000000000000000, 0.000000000000000000, 0.000000000000000000 ) ) ;
#5651=UNCERTAINTY_MEASURE_WITH_UNIT (LENGTH_MEASURE( 1.000000000000000082E-05 ), #224, 'distance_accuracy_value', 'NONE') ;
#5713=DIRECTION ( 'NONE',  ( -1.000000000000000000, 0.000000000000000000, 0.000000000000000000 ) ) ;
#5760=( BOUNDED_CURVE ( )  B_SPLINE_CURVE ( 2, ( #5803, #3656, #1689 ),
 .UNSPECIFIED., .F., .T. ) 
 B_SPLINE_CURVE_WITH_KNOTS ( ( 3, 3 ),
 ( 0.000000000000000000, 0.5842180690389568998 ),
 .UNSPECIFIED. ) 
 CURVE ( )  GEOMETRIC_REPRESENTATION_ITEM ( )  RATIONAL_B_SPLINE_CURVE ( ( 1.000000000000000000, 1.154700538379249908, 1.000000000000000000 ) ) 
 REPRESENTATION_ITEM ( '' )  ) ;
#5788=ORIENTED_EDGE ( 'NONE', *, *, #19691, .T. ) ;
#5803=CARTESIAN_POINT ( 'NONE',  ( 0.03008364706454716778, -0.1136516277932324709, -0.1968503937007874127 ) ) ;
#5858=ORIENTED_EDGE ( 'NONE', *, *, #10075, .T. ) ;
#5937=CARTESIAN_POINT ( 'NONE',  ( 0.09590060490395689585, 0.2273032555864669124, 0.000000000000000000 ) ) ;
#5939=FACE_BOUND ( 'NONE', #22118, .T. ) ;
#5975=ORIENTED_EDGE ( 'NONE', *, *, #24525, .F. ) ;
#5988=CARTESIAN_POINT ( 'NONE',  ( 0.09590060490395689585, 0.1136516277932340530, -0.1968503937007874127 ) ) ;
#6119=CARTESIAN_POINT ( 'NONE',  ( 0.01504182353227358389, 0.2012500529900838608, 0.000000000000000000 ) ) ;
#6307=ORIENTED_EDGE ( 'NONE', *, *, #18039, .T. ) ;
#6373=DIRECTION ( 'NONE',  ( 0.000000000000000000, 0.000000000000000000, 1.000000000000000000 ) ) ;
#6383=LINE ( 'NONE', #6119, #722 ) ;
#6430=CARTESIAN_POINT ( 'NONE',  ( 0.09590060490395689585, 0.2273032555864669124, 0.000000000000000000 ) ) ;
#6444=FACE_OUTER_BOUND ( 'NONE', #25099, .T. ) ;
#6468=ORIENTED_EDGE ( 'NONE', *, *, #24717, .F. ) ;
#6473=EDGE_LOOP ( 'NONE', ( #11151, #3057, #6307, #14316 ) ) ;
#6514=CARTESIAN_POINT ( 'NONE',  ( 0.03008364706454716778, -0.2273032555864669124, 2.185478346456692557E-17 ) ) ;
#6675=ORIENTED_EDGE ( 'NONE', *, *, #27515, .T. ) ;
#6731=CARTESIAN_POINT ( 'NONE',  ( 0.000000000000000000, 0.000000000000000000, 0.000000000000000000 ) ) ;
#6734=ADVANCED_FACE ( 'NONE', ( #9730 ), #9574, .T. ) ;
#6789=DIRECTION ( 'NONE',  ( -1.000000000000000000, 0.000000000000000000, 0.000000000000000000 ) ) ;
#6827=( NAMED_UNIT ( * ) PLANE_ANGLE_UNIT ( ) SI_UNIT ( $, .RADIAN. ) ) ;
#6891=VERTEX_POINT ( 'NONE', #7767 ) ;
#6907=DIRECTION ( 'NONE',  ( -1.000000000000000000, 0.000000000000000000, 0.000000000000000000 ) ) ;
#6965=( LENGTH_UNIT ( ) NAMED_UNIT ( * ) SI_UNIT ( $, .METRE. ) ) ;
#7108=EDGE_CURVE ( 'NONE', #12714, #13350, #12641, .T. ) ;
#7114=PRODUCT_DEFINITION_FORMATION_WITH_SPECIFIED_SOURCE ( 'ANY', '', #163, .NOT_KNOWN. ) ;
#7170=VECTOR ( 'NONE', #26388, 39.37007874015748854 ) ;
#7213=CYLINDRICAL_SURFACE ( 'NONE', #302, 0.09679133858267717494 ) ;
#7220=DIMENSIONAL_EXPONENTS ( 1.000000000000000000, 0.000000000000000000, 0.000000000000000000, 0.000000000000000000, 0.000000000000000000, 0.000000000000000000, 0.000000000000000000 ) ;
#7309=ADVANCED_FACE ( 'NONE', ( #25970 ), #19883, .T. ) ;
#7462=ORIENTED_EDGE ( 'NONE', *, *, #8151, .F. ) ;
#7530=ADVANCED_FACE ( 'NONE', ( #18431 ), #12518, .F. ) ;
#7636=CARTESIAN_POINT ( 'NONE',  ( 0.000000000000000000, 0.2273032555864669124, 9.010881889763779798E-17 ) ) ;
#7715=CIRCLE ( 'NONE', #23522, 0.1181010187939084827 ) ;
#7749=CONICAL_SURFACE ( 'NONE', #970, 0.1074461786882927178, 1.047197550000000144 ) ;
#7767=CARTESIAN_POINT ( 'NONE',  ( 0.000000000000000000, 0.000000000000000000, -0.1181010187644645215 ) ) ;
#7830=LINE ( 'NONE', #20113, #5400 ) ;
#7889=CARTESIAN_POINT ( 'NONE',  ( 0.1259842519685039353, -0.1751968503937007815, -2.466516690495447540E-17 ) ) ;
#7908=AXIS2_PLACEMENT_3D ( 'NONE', #27376, #20735, #27234 ) ;
#7918=CARTESIAN_POINT ( 'NONE',  ( 0.000000000000000000, -0.1136516277932334562, 0.1968503937007874127 ) ) ;
#7919=CARTESIAN_POINT ( 'NONE',  ( 0.000000000000000000, -0.1751968503937007815, 2.466516690495447540E-17 ) ) ;
#7921=EDGE_CURVE ( 'NONE', #3844, #11261, #21266, .T. ) ;
#7923=DIRECTION ( 'NONE',  ( 1.000000000000000000, 0.000000000000000000, 0.000000000000000000 ) ) ;
#7967=CARTESIAN_POINT ( 'NONE',  ( 0.1136811023622047168, 0.000000000000000000, 0.000000000000000000 ) ) ;
#8001=EDGE_CURVE ( 'NONE', #13350, #657, #12194, .T. ) ;
#8018=ADVANCED_FACE ( 'NONE', ( #10206 ), #7749, .F. ) ;
#8037=ORIENTED_EDGE ( 'NONE', *, *, #3659, .T. ) ;
#8063=FACE_OUTER_BOUND ( 'NONE', #6473, .T. ) ;
#8110=DIRECTION ( 'NONE',  ( 1.000000000000000000, 0.000000000000000000, 0.000000000000000000 ) ) ;
#8151=EDGE_CURVE ( 'NONE', #15134, #8851, #8248, .T. ) ;
#8170=ORIENTED_EDGE ( 'NONE', *, *, #7921, .T. ) ;
#8223=ORIENTED_EDGE ( 'NONE', *, *, #19267, .T. ) ;
#8248=LINE ( 'NONE', #14909, #25321 ) ;
#8287=ORIENTED_EDGE ( 'NONE', *, *, #22387, .T. ) ;
#8303=ORIENTED_EDGE ( 'NONE', *, *, #13257, .F. ) ;
#8324=AXIS2_PLACEMENT_3D ( 'NONE', #721, #22047, #4546 ) ;
#8385=CARTESIAN_POINT ( 'NONE',  ( 0.09590060490395689585, 0.1136516277932334562, 0.1968503937007874127 ) ) ;
#8494=ORIENTED_EDGE ( 'NONE', *, *, #13983, .T. ) ;
#8526=PRESENTATION_STYLE_ASSIGNMENT (( #93 ) ) ;
#8632=( BOUNDED_CURVE ( )  B_SPLINE_CURVE ( 2, ( #15446, #23644, #21375 ),
 .UNSPECIFIED., .F., .T. ) 
 B_SPLINE_CURVE_WITH_KNOTS ( ( 3, 3 ),
 ( 0.000000000000000000, 0.5842180690389588982 ),
 .UNSPECIFIED. ) 
 CURVE ( )  GEOMETRIC_REPRESENTATION_ITEM ( )  RATIONAL_B_SPLINE_CURVE ( ( 1.000000000000000000, 1.154700538379251906, 1.000000000000000000 ) ) 
 REPRESENTATION_ITEM ( '' )  ) ;
#8663=DIRECTION ( 'NONE',  ( 1.000000000000000000, 0.000000000000000000, 0.000000000000000000 ) ) ;
#8851=VERTEX_POINT ( 'NONE', #6514 ) ;
#8864=EDGE_CURVE ( 'NONE', #11261, #20886, #1853, .T. ) ;
#8872=VECTOR ( 'NONE', #1329, 39.37007874015748143 ) ;
#8916=EDGE_LOOP ( 'NONE', ( #26631, #368, #6675, #10235 ) ) ;
#8931=LENGTH_MEASURE_WITH_UNIT ( LENGTH_MEASURE( 0.02539999999999999897 ), #6965 ) ;
#8962=AXIS2_PLACEMENT_3D ( 'NONE', #18340, #23034, #14135 ) ;
#8977=ORIENTED_EDGE ( 'NONE', *, *, #10512, .T. ) ;
#9001=EDGE_LOOP ( 'NONE', ( #23203, #5858, #9564, #12891, #560, #27568 ) ) ;
#9027=EDGE_LOOP ( 'NONE', ( #2348, #1849, #26966, #5414 ) ) ;
#9032=DIRECTION ( 'NONE',  ( 0.5000000010362839475, -0.8660254031861397417, 1.060575237992202059E-16 ) ) ;
#9082=CARTESIAN_POINT ( 'NONE',  ( 0.000000000000000000, -1.446320346059429855E-17, 0.1181010187644645215 ) ) ;
#9083=CARTESIAN_POINT ( 'NONE',  ( 0.09590060490395689585, 0.1136516277932340530, -0.1968503937007874127 ) ) ;
#9106=DIRECTION ( 'NONE',  ( 0.000000000000000000, 0.000000000000000000, 1.000000000000000000 ) ) ;
#9150=LINE ( 'NONE', #17770, #7170 ) ;
#9213=CONICAL_SURFACE ( 'NONE', #24123, 0.1074461786882927178, 1.047197550000000144 ) ;
#9293=CIRCLE ( 'NONE', #20137, 0.09679133858267717494 ) ;
#9362=DIRECTION ( 'NONE',  ( 0.000000000000000000, 1.000000000000000000, 0.000000000000000000 ) ) ;
#9496=VERTEX_POINT ( 'NONE', #11504 ) ;
#9564=ORIENTED_EDGE ( 'NONE', *, *, #18039, .F. ) ;
#9574=PLANE ( 'NONE',  #13535 ) ;
#9652=DIRECTION ( 'NONE',  ( 1.000000000000000000, 0.000000000000000000, 0.000000000000000000 ) ) ;
#9730=FACE_OUTER_BOUND ( 'NONE', #15, .T. ) ;
#9744=PLANE ( 'NONE',  #3807 ) ;
#9876=ORIENTED_EDGE ( 'NONE', *, *, #18551, .T. ) ;
#9881=LINE ( 'NONE', #24567, #2395 ) ;
#9951=ORIENTED_EDGE ( 'NONE', *, *, #13257, .T. ) ;
#10075=EDGE_CURVE ( 'NONE', #2155, #18698, #16695, .T. ) ;
#10206=FACE_OUTER_BOUND ( 'NONE', #13779, .T. ) ;
#10235=ORIENTED_EDGE ( 'NONE', *, *, #27618, .F. ) ;
#10415=FACE_OUTER_BOUND ( 'NONE', #26359, .T. ) ;
#10479=ADVANCED_FACE ( 'NONE', ( #10415 ), #15460, .T. ) ;
#10501=UNCERTAINTY_MEASURE_WITH_UNIT (LENGTH_MEASURE( 1.000000000000000082E-05 ), #23442, 'distance_accuracy_value', 'NONE') ;
#10512=EDGE_CURVE ( 'NONE', #13350, #2437, #19316, .T. ) ;
#10587=CARTESIAN_POINT ( 'NONE',  ( 0.03008364706454716778, 0.1136516277932334562, 0.1968503937007874127 ) ) ;
#10707=ORIENTED_EDGE ( 'NONE', *, *, #7921, .F. ) ;
#10718=EDGE_CURVE ( 'NONE', #15474, #11206, #1957, .T. ) ;
#10895=DIRECTION ( 'NONE',  ( -0.5000000010362839475, 0.8660254031861397417, 0.000000000000000000 ) ) ;
#10992=CLOSED_SHELL ( 'NONE', ( #14896, #7530, #1466, #23241, #7309, #23008, #5261, #673, #6734, #19617, #737, #14132, #10479, #24149, #8018, #12943, #26471, #25138 ) ) ;
#11046=AXIS2_PLACEMENT_3D ( 'NONE', #13486, #2613, #9106 ) ;
#11151=ORIENTED_EDGE ( 'NONE', *, *, #2073, .T. ) ;
#11178=DIRECTION ( 'NONE',  ( 1.000000000000000000, 0.000000000000000000, 0.000000000000000000 ) ) ;
#11206=VERTEX_POINT ( 'NONE', #8385 ) ;
#11261=VERTEX_POINT ( 'NONE', #24182 ) ;
#11274=DIRECTION ( 'NONE',  ( 0.000000000000000000, 1.000000000000000000, 0.000000000000000000 ) ) ;
#11413=CARTESIAN_POINT ( 'NONE',  ( -0.002724751885584173784, -0.1704774416898503786, -0.09842519685039387289 ) ) ;
#11504=CARTESIAN_POINT ( 'NONE',  ( 0.03008364706454716778, -0.1136516277932324709, -0.1968503937007874127 ) ) ;
#11511=PRODUCT_CONTEXT ( 'NONE', #14882, 'mechanical' ) ;
#11555=ORIENTED_EDGE ( 'NONE', *, *, #24176, .F. ) ;
#11588=AXIS2_PLACEMENT_3D ( 'NONE', #5229, #3665, #7923 ) ;
#11677=( BOUNDED_CURVE ( )  B_SPLINE_CURVE ( 2, ( #6430, #17575, #9083 ),
 .UNSPECIFIED., .F., .F. ) 
 B_SPLINE_CURVE_WITH_KNOTS ( ( 3, 3 ),
 ( 0.000000000000000000, 0.5842180690389578990 ),
 .UNSPECIFIED. ) 
 CURVE ( )  GEOMETRIC_REPRESENTATION_ITEM ( )  RATIONAL_B_SPLINE_CURVE ( ( 1.000000000000000000, 1.154700538379245911, 1.000000000000000000 ) ) 
 REPRESENTATION_ITEM ( '' )  ) ;
#11725=CIRCLE ( 'NONE', #27063, 0.1751968503937007815 ) ;
#11858=ORIENTED_EDGE ( 'NONE', *, *, #20245, .T. ) ;
#11863=DIRECTION ( 'NONE',  ( 1.000000000000000000, 0.000000000000000000, 0.000000000000000000 ) ) ;
#11889=PRODUCT_DEFINITION ( 'UNKNOWN', '', #7114, #20685 ) ;
#11923=DIRECTION ( 'NONE',  ( 0.000000000000000000, 0.000000000000000000, 1.000000000000000000 ) ) ;
#12050=CARTESIAN_POINT ( 'NONE',  ( 0.000000000000000000, 0.000000000000000000, 0.000000000000000000 ) ) ;
#12142=DIRECTION ( 'NONE',  ( -1.000000000000000000, 0.000000000000000000, 0.000000000000000000 ) ) ;
#12151=APPLICATION_CONTEXT ( 'automotive_design' ) ;
#12194=LINE ( 'NONE', #23089, #20361 ) ;
#12195=ORIENTED_EDGE ( 'NONE', *, *, #24359, .F. ) ;
#12203=CARTESIAN_POINT ( 'NONE',  ( 0.1259842519685039353, 0.000000000000000000, 0.1181010187644645354 ) ) ;
#12223=DIRECTION ( 'NONE',  ( 0.000000000000000000, 0.000000000000000000, -1.000000000000000000 ) ) ;
#12234=CARTESIAN_POINT ( 'NONE',  ( -0.4895985792973480133, 0.000000000000000000, 0.000000000000000000 ) ) ;
#12242=EDGE_CURVE ( 'NONE', #6891, #2437, #7715, .T. ) ;
#12377=( BOUNDED_CURVE ( )  B_SPLINE_CURVE ( 2, ( #18620, #3648, #5937 ),
 .UNSPECIFIED., .F., .F. ) 
 B_SPLINE_CURVE_WITH_KNOTS ( ( 3, 3 ),
 ( 0.000000000000000000, 0.5842180690389588982 ),
 .UNSPECIFIED. ) 
 CURVE ( )  GEOMETRIC_REPRESENTATION_ITEM ( )  RATIONAL_B_SPLINE_CURVE ( ( 1.000000000000000000, 1.154700538379253905, 1.000000000000000000 ) ) 
 REPRESENTATION_ITEM ( '' )  ) ;
#12389=ORIENTED_EDGE ( 'NONE', *, *, #16621, .T. ) ;
#12518=CYLINDRICAL_SURFACE ( 'NONE', #14014, 0.09679133858267717494 ) ;
#12544=VERTEX_POINT ( 'NONE', #4027 ) ;
#12641=CIRCLE ( 'NONE', #24348, 0.09679133858267717494 ) ;
#12644=DIRECTION ( 'NONE',  ( 0.000000000000000000, -1.000000000000000000, 0.000000000000000000 ) ) ;
#12714=VERTEX_POINT ( 'NONE', #20383 ) ;
#12731=LINE ( 'NONE', #21639, #17931 ) ;
#12891=ORIENTED_EDGE ( 'NONE', *, *, #19240, .F. ) ;
#12935=EDGE_LOOP ( 'NONE', ( #8170, #21850, #5788, #3933 ) ) ;
#12943=ADVANCED_FACE ( 'NONE', ( #15819, #1507 ), #22993, .F. ) ;
#12964=DIRECTION ( 'NONE',  ( 0.000000000000000000, 0.000000000000000000, -1.000000000000000000 ) ) ;
#13041=ORIENTED_EDGE ( 'NONE', *, *, #27618, .T. ) ;
#13107=DIRECTION ( 'NONE',  ( 1.000000000000000000, 0.000000000000000000, 0.000000000000000000 ) ) ;
#13110=EDGE_LOOP ( 'NONE', ( #3635, #2785, #22657, #1846, #13648, #13464 ) ) ;
#13157=FACE_OUTER_BOUND ( 'NONE', #8916, .T. ) ;
#13216=DIRECTION ( 'NONE',  ( -1.000000000000000000, 0.000000000000000000, 0.000000000000000000 ) ) ;
#13257=EDGE_CURVE ( 'NONE', #2437, #6891, #18596, .T. ) ;
#13316=LINE ( 'NONE', #229, #2182 ) ;
#13350=VERTEX_POINT ( 'NONE', #13727 ) ;
#13409=CARTESIAN_POINT ( 'NONE',  ( 0.03008364706454716778, -0.1136516277932334562, 0.1968503937007874127 ) ) ;
#13464=ORIENTED_EDGE ( 'NONE', *, *, #2564, .F. ) ;
#13486=CARTESIAN_POINT ( 'NONE',  ( 0.1198326771653543399, 0.000000000000000000, 0.000000000000000000 ) ) ;
#13535=AXIS2_PLACEMENT_3D ( 'NONE', #20049, #22590, #1128 ) ;
#13648=ORIENTED_EDGE ( 'NONE', *, *, #20014, .F. ) ;
#13650=DIRECTION ( 'NONE',  ( 0.000000000000000000, -0.8660254037844388186, 0.4999999999999998890 ) ) ;
#13685=AXIS2_PLACEMENT_3D ( 'NONE', #26246, #6907, #11274 ) ;
#13705=VECTOR ( 'NONE', #24992, 39.37007874015748143 ) ;
#13727=CARTESIAN_POINT ( 'NONE',  ( 0.01230314960629921330, 1.185352029804633059E-17, 0.09679133858267717494 ) ) ;
#13779=EDGE_LOOP ( 'NONE', ( #3443, #26971, #5013, #4355 ) ) ;
#13804=EDGE_CURVE ( 'NONE', #26100, #26154, #9881, .T. ) ;
#13844=ORIENTED_EDGE ( 'NONE', *, *, #24176, .T. ) ;
#13860=ORIENTED_EDGE ( 'NONE', *, *, #10075, .F. ) ;
#13897=LINE ( 'NONE', #18096, #8872 ) ;
#13983=EDGE_CURVE ( 'NONE', #2155, #19119, #1513, .T. ) ;
#14014=AXIS2_PLACEMENT_3D ( 'NONE', #12234, #16758, #14372 ) ;
#14132=ADVANCED_FACE ( 'NONE', ( #17759 ), #25434, .T. ) ;
#14133=CARTESIAN_POINT ( 'NONE',  ( 0.03008364706454716778, -0.1136516277932328595, -0.1968503937007874127 ) ) ;
#14135=DIRECTION ( 'NONE',  ( 0.000000000000000000, 0.5000000000000003331, -0.8660254037844384856 ) ) ;
#14167=AXIS2_PLACEMENT_3D ( 'NONE', #25278, #19051, #18623 ) ;
#14316=ORIENTED_EDGE ( 'NONE', *, *, #3659, .F. ) ;
#14372=DIRECTION ( 'NONE',  ( 0.000000000000000000, 0.000000000000000000, -1.000000000000000000 ) ) ;
#14413=EDGE_CURVE ( 'NONE', #26100, #657, #24078, .T. ) ;
#14428=FACE_OUTER_BOUND ( 'NONE', #4746, .T. ) ;
#14468=CARTESIAN_POINT ( 'NONE',  ( -0.002724751885584056257, 0.1704774416898501010, 0.09842519685039388677 ) ) ;
#14557=ORIENTED_EDGE ( 'NONE', *, *, #1228, .F. ) ;
#14574=CARTESIAN_POINT ( 'NONE',  ( 0.1259842519685039353, 4.470295275590551256E-17, -8.195543307086614694E-17 ) ) ;
#14603=( BOUNDED_CURVE ( )  B_SPLINE_CURVE ( 2, ( #10587, #17011, #4434 ),
 .UNSPECIFIED., .F., .F. ) 
 B_SPLINE_CURVE_WITH_KNOTS ( ( 3, 3 ),
 ( 0.000000000000000000, 0.5842180690389588982 ),
 .UNSPECIFIED. ) 
 CURVE ( )  GEOMETRIC_REPRESENTATION_ITEM ( )  RATIONAL_B_SPLINE_CURVE ( ( 1.000000000000000000, 1.154700538379251906, 1.000000000000000000 ) ) 
 REPRESENTATION_ITEM ( '' )  ) ;
#14618=ORIENTED_EDGE ( 'NONE', *, *, #23655, .T. ) ;
#14722=DIRECTION ( 'NONE',  ( 1.000000000000000000, 0.000000000000000000, 0.000000000000000000 ) ) ;
#14869=CARTESIAN_POINT ( 'NONE',  ( 0.1287090038540879000, 4.133240157480319260E-16, -0.1968503937007877458 ) ) ;
#14882=APPLICATION_CONTEXT ( 'automotive_design' ) ;
#14896=ADVANCED_FACE ( 'NONE', ( #19520 ), #25455, .F. ) ;
#14909=CARTESIAN_POINT ( 'NONE',  ( 0.01504182353227358389, -0.2012500529900838608, 2.464602332225414408E-17 ) ) ;
#14915=CARTESIAN_POINT ( 'NONE',  ( 0.000000000000000000, 0.1751968503937007815, 0.000000000000000000 ) ) ;
#14953=EDGE_LOOP ( 'NONE', ( #15504, #8977, #9951, #19145 ) ) ;
#15102=LENGTH_MEASURE_WITH_UNIT ( LENGTH_MEASURE( 0.02539999999999999897 ), #3784 ) ;
#15110=ORIENTED_EDGE ( 'NONE', *, *, #3666, .F. ) ;
#15115=CARTESIAN_POINT ( 'NONE',  ( 0.01230314960629921330, 0.000000000000000000, 0.000000000000000000 ) ) ;
#15134=VERTEX_POINT ( 'NONE', #7919 ) ;
#15140=CIRCLE ( 'NONE', #7908, 0.1181010187939084827 ) ;
#15423=DIRECTION ( 'NONE',  ( 0.000000000000000000, 1.000000000000000000, 0.000000000000000000 ) ) ;
#15446=CARTESIAN_POINT ( 'NONE',  ( 0.03008364706454716778, -0.1136516277932334562, 0.1968503937007874127 ) ) ;
#15460=CONICAL_SURFACE ( 'NONE', #19047, 0.2012500529900838608, 1.047197550000000144 ) ;
#15465=AXIS2_PLACEMENT_3D ( 'NONE', #26535, #1367, #3611 ) ;
#15474=VERTEX_POINT ( 'NONE', #20772 ) ;
#15504=ORIENTED_EDGE ( 'NONE', *, *, #7108, .T. ) ;
#15591=CARTESIAN_POINT ( 'NONE',  ( 0.03008364706454716778, -0.2273032555864669124, 3.963736220472441631E-17 ) ) ;
#15695=( GEOMETRIC_REPRESENTATION_CONTEXT ( 3 ) GLOBAL_UNCERTAINTY_ASSIGNED_CONTEXT ( ( #10501 ) ) GLOBAL_UNIT_ASSIGNED_CONTEXT ( ( #23442, #21307, #25543 ) ) REPRESENTATION_CONTEXT ( 'NONE', 'WORKASPACE' ) ) ;
#15703=DIRECTION ( 'NONE',  ( 0.000000000000000000, 0.000000000000000000, -1.000000000000000000 ) ) ;
#15773=CIRCLE ( 'NONE', #21186, 0.1181010187939084827 ) ;
#15819=FACE_BOUND ( 'NONE', #3436, .T. ) ;
#15970=CARTESIAN_POINT ( 'NONE',  ( 0.1136811023622047168, 0.000000000000000000, 0.09679133858267717494 ) ) ;
#16232=SHAPE_REPRESENTATION ( 'M6 Thin Hex Nut', ( #11588 ), #15695 ) ;
#16276=ORIENTED_EDGE ( 'NONE', *, *, #5317, .T. ) ;
#16293=ORIENTED_EDGE ( 'NONE', *, *, #16737, .T. ) ;
#16306=DIRECTION ( 'NONE',  ( 1.000000000000000000, 0.000000000000000000, 0.000000000000000000 ) ) ;
#16369=CARTESIAN_POINT ( 'NONE',  ( 0.09590060490395689585, -0.2273032555864669124, 2.185478346456692557E-17 ) ) ;
#16427=CARTESIAN_POINT ( 'NONE',  ( 0.03008364706454716778, 0.2273032555864669124, 0.000000000000000000 ) ) ;
#16495=ORIENTED_EDGE ( 'NONE', *, *, #10718, .T. ) ;
#16621=EDGE_CURVE ( 'NONE', #15134, #3577, #11725, .T. ) ;
#16629=DIRECTION ( 'NONE',  ( -1.000000000000000000, 0.000000000000000000, 0.000000000000000000 ) ) ;
#16670=CARTESIAN_POINT ( 'NONE',  ( 0.03008364706454716778, -0.1136516277932334562, 0.1968503937007874127 ) ) ;
#16695=LINE ( 'NONE', #25015, #2385 ) ;
#16737=EDGE_CURVE ( 'NONE', #18698, #15474, #31, .T. ) ;
#16758=DIRECTION ( 'NONE',  ( 1.000000000000000000, 0.000000000000000000, 0.000000000000000000 ) ) ;
#16840=EDGE_LOOP ( 'NONE', ( #16276, #19733, #26817, #2117 ) ) ;
#16904=FACE_OUTER_BOUND ( 'NONE', #13110, .T. ) ;
#16910=EDGE_CURVE ( 'NONE', #3844, #24509, #7830, .T. ) ;
#16960=DIRECTION ( 'NONE',  ( 1.000000000000000000, 0.000000000000000000, 0.000000000000000000 ) ) ;
#16964=CARTESIAN_POINT ( 'NONE',  ( 0.09590060490395689585, 0.1136516277932340530, -0.1968503937007874127 ) ) ;
#17011=CARTESIAN_POINT ( 'NONE',  ( -0.002724751885584093553, 0.000000000000000000, 0.1968503937007874127 ) ) ;
#17218=DIRECTION ( 'NONE',  ( 0.000000000000000000, 1.000000000000000000, 0.000000000000000000 ) ) ;
#17355=CARTESIAN_POINT ( 'NONE',  ( 0.1287090038540882331, -0.1704774416898503786, -0.09842519685039387289 ) ) ;
#17575=CARTESIAN_POINT ( 'NONE',  ( 0.1287090038540880110, 0.1704774416898509615, -0.09842519685039369248 ) ) ;
#17596=VERTEX_POINT ( 'NONE', #13409 ) ;
#17623=CARTESIAN_POINT ( 'NONE',  ( 0.09590060490395689585, -0.1136516277932324709, -0.1968503937007874127 ) ) ;
#17759=FACE_OUTER_BOUND ( 'NONE', #18696, .T. ) ;
#17770=CARTESIAN_POINT ( 'NONE',  ( 0.006151574803149606648, 0.000000000000000000, -0.1074461786882927178 ) ) ;
#17843=CARTESIAN_POINT ( 'NONE',  ( -0.002724751885583937862, 0.1704774416898503786, -0.09842519685039353983 ) ) ;
#17931=VECTOR ( 'NONE', #10895, 39.37007874015748854 ) ;
#18039=EDGE_CURVE ( 'NONE', #25577, #18698, #23033, .T. ) ;
#18045=LINE ( 'NONE', #14133, #26333 ) ;
#18096=CARTESIAN_POINT ( 'NONE',  ( -0.4895985792973480133, 0.000000000000000000, -0.09679133858267717494 ) ) ;
#18340=CARTESIAN_POINT ( 'NONE',  ( 0.000000000000000000, -0.1136516277932328595, -0.1968503937007874127 ) ) ;
#18343=( BOUNDED_CURVE ( )  B_SPLINE_CURVE ( 2, ( #22151, #11413, #24539 ),
 .UNSPECIFIED., .F., .F. ) 
 B_SPLINE_CURVE_WITH_KNOTS ( ( 3, 3 ),
 ( 0.000000000000000000, 0.5842180690389598974 ),
 .UNSPECIFIED. ) 
 CURVE ( )  GEOMETRIC_REPRESENTATION_ITEM ( )  RATIONAL_B_SPLINE_CURVE ( ( 1.000000000000000000, 1.154700538379249908, 1.000000000000000000 ) ) 
 REPRESENTATION_ITEM ( '' )  ) ;
#18409=STYLED_ITEM ( 'NONE', ( #8526 ), #3447 ) ;
#18431=FACE_OUTER_BOUND ( 'NONE', #9027, .T. ) ;
#18541=DIRECTION ( 'NONE',  ( 1.000000000000000000, 0.000000000000000000, 0.000000000000000000 ) ) ;
#18551=EDGE_CURVE ( 'NONE', #12714, #6891, #9150, .T. ) ;
#18596=CIRCLE ( 'NONE', #3262, 0.1181010187939084827 ) ;
#18620=CARTESIAN_POINT ( 'NONE',  ( 0.09590060490395689585, 0.1136516277932334562, 0.1968503937007874127 ) ) ;
#18623=DIRECTION ( 'NONE',  ( 0.000000000000000000, 1.000000000000000000, 0.000000000000000000 ) ) ;
#18626=PLANE ( 'NONE',  #23218 ) ;
#18676=CIRCLE ( 'NONE', #27729, 0.1751968503937007815 ) ;
#18696=EDGE_LOOP ( 'NONE', ( #13860, #6468, #1106, #1597, #3025, #23671 ) ) ;
#18698=VERTEX_POINT ( 'NONE', #16369 ) ;
#18823=CARTESIAN_POINT ( 'NONE',  ( 0.1198326771653543399, 0.000000000000000000, 0.000000000000000000 ) ) ;
#18982=DIMENSIONAL_EXPONENTS ( 1.000000000000000000, 0.000000000000000000, 0.000000000000000000, 0.000000000000000000, 0.000000000000000000, 0.000000000000000000, 0.000000000000000000 ) ;
#19047=AXIS2_PLACEMENT_3D ( 'NONE', #4489, #149, #2350 ) ;
#19051=DIRECTION ( 'NONE',  ( 1.000000000000000000, 0.000000000000000000, 0.000000000000000000 ) ) ;
#19052=LINE ( 'NONE', #16670, #13705 ) ;
#19119=VERTEX_POINT ( 'NONE', #183 ) ;
#19145=ORIENTED_EDGE ( 'NONE', *, *, #18551, .F. ) ;
#19240=EDGE_CURVE ( 'NONE', #24509, #25577, #2827, .T. ) ;
#19267=EDGE_CURVE ( 'NONE', #12544, #17596, #14603, .T. ) ;
#19316=LINE ( 'NONE', #1944, #4600 ) ;
#19323=( GEOMETRIC_REPRESENTATION_CONTEXT ( 3 ) GLOBAL_UNCERTAINTY_ASSIGNED_CONTEXT ( ( #5651 ) ) GLOBAL_UNIT_ASSIGNED_CONTEXT ( ( #224, #6827, #21797 ) ) REPRESENTATION_CONTEXT ( 'NONE', 'WORKASPACE' ) ) ;
#19349=ORIENTED_EDGE ( 'NONE', *, *, #2073, .F. ) ;
#19462=ORIENTED_EDGE ( 'NONE', *, *, #24717, .T. ) ;
#19519=PRODUCT_DEFINITION_SHAPE ( 'NONE', 'NONE',  #11889 ) ;
#19520=FACE_OUTER_BOUND ( 'NONE', #14953, .T. ) ;
#19617=ADVANCED_FACE ( 'NONE', ( #23540 ), #3594, .T. ) ;
#19691=EDGE_CURVE ( 'NONE', #20886, #24509, #11677, .T. ) ;
#19733=ORIENTED_EDGE ( 'NONE', *, *, #16910, .T. ) ;
#19773=CARTESIAN_POINT ( 'NONE',  ( 0.000000000000000000, 0.000000000000000000, 0.000000000000000000 ) ) ;
#19883=CONICAL_SURFACE ( 'NONE', #73, 0.2012500529900838608, 1.047197550000000144 ) ;
#19918=CARTESIAN_POINT ( 'NONE',  ( 0.1259842519685039353, -1.446320346059429855E-17, -0.1181010187644645354 ) ) ;
#20014=EDGE_CURVE ( 'NONE', #11261, #12544, #26127, .T. ) ;
#20040=AXIS2_PLACEMENT_3D ( 'NONE', #27370, #16629, #23285 ) ;
#20043=AXIS2_PLACEMENT_3D ( 'NONE', #24986, #5647, #17218 ) ;
#20049=CARTESIAN_POINT ( 'NONE',  ( 0.000000000000000000, 0.1136516277932332619, 0.1968503937007874127 ) ) ;
#20113=CARTESIAN_POINT ( 'NONE',  ( 0.03008364706454716778, 0.1136516277932338587, -0.1968503937007874127 ) ) ;
#20126=SHAPE_DEFINITION_REPRESENTATION ( #19519, #16232 ) ;
#20137=AXIS2_PLACEMENT_3D ( 'NONE', #7967, #5713, #6373 ) ;
#20221=COLOUR_RGB ( '', 0.72549020, 0.75294118, 0.79215686) ;
#20245=EDGE_CURVE ( 'NONE', #17596, #8851, #8632, .T. ) ;
#20361=VECTOR ( 'NONE', #18541, 39.37007874015748143 ) ;
#20383=CARTESIAN_POINT ( 'NONE',  ( 0.01230314960629921330, 0.000000000000000000, -0.09679133858267717494 ) ) ;
#20472=CIRCLE ( 'NONE', #227, 0.09679133858267717494 ) ;
#20627=PLANE ( 'NONE',  #8962 ) ;
#20685=PRODUCT_DEFINITION_CONTEXT ( 'detailed design', #12151, 'design' ) ;
#20714=FACE_OUTER_BOUND ( 'NONE', #1448, .T. ) ;
#20735=DIRECTION ( 'NONE',  ( 1.000000000000000000, 0.000000000000000000, 0.000000000000000000 ) ) ;
#20769=ORIENTED_EDGE ( 'NONE', *, *, #24166, .T. ) ;
#20772=CARTESIAN_POINT ( 'NONE',  ( 0.09590060490395689585, -0.1136516277932334562, 0.1968503937007874127 ) ) ;
#20886=VERTEX_POINT ( 'NONE', #21692 ) ;
#21121=ORIENTED_EDGE ( 'NONE', *, *, #12242, .F. ) ;
#21186=AXIS2_PLACEMENT_3D ( 'NONE', #21340, #16960, #4105 ) ;
#21230=EDGE_LOOP ( 'NONE', ( #19462, #8494 ) ) ;
#21236=DIRECTION ( 'NONE',  ( 0.000000000000000000, 1.000000000000000000, 0.000000000000000000 ) ) ;
#21266=( BOUNDED_CURVE ( )  B_SPLINE_CURVE ( 2, ( #24621, #17843, #2464 ),
 .UNSPECIFIED., .F., .T. ) 
 B_SPLINE_CURVE_WITH_KNOTS ( ( 3, 3 ),
 ( 0.000000000000000000, 0.5842180690389578990 ),
 .UNSPECIFIED. ) 
 CURVE ( )  GEOMETRIC_REPRESENTATION_ITEM ( )  RATIONAL_B_SPLINE_CURVE ( ( 1.000000000000000000, 1.154700538379249908, 1.000000000000000000 ) ) 
 REPRESENTATION_ITEM ( '' )  ) ;
#21307=( NAMED_UNIT ( * ) PLANE_ANGLE_UNIT ( ) SI_UNIT ( $, .RADIAN. ) ) ;
#21340=CARTESIAN_POINT ( 'NONE',  ( 0.1259842519685039353, 0.000000000000000000, 0.000000000000000000 ) ) ;
#21375=CARTESIAN_POINT ( 'NONE',  ( 0.03008364706454716778, -0.2273032555864669124, 2.185478346456692557E-17 ) ) ;
#21593=DIRECTION ( 'NONE',  ( -1.000000000000000000, 0.000000000000000000, 0.000000000000000000 ) ) ;
#21639=CARTESIAN_POINT ( 'NONE',  ( 0.1109424284362303254, 0.2012500529900838608, 0.000000000000000000 ) ) ;
#21692=CARTESIAN_POINT ( 'NONE',  ( 0.09590060490395689585, 0.2273032555864669124, 0.000000000000000000 ) ) ;
#21770=CARTESIAN_POINT ( 'NONE',  ( 0.1136811023622047168, -1.315836188112323537E-17, -0.09679133858267717494 ) ) ;
#21797=( NAMED_UNIT ( * ) SI_UNIT ( $, .STERADIAN. ) SOLID_ANGLE_UNIT ( ) ) ;
#21809=AXIS2_PLACEMENT_3D ( 'NONE', #5031, #13650, #3317 ) ;
#21850=ORIENTED_EDGE ( 'NONE', *, *, #8864, .T. ) ;
#21944=DIRECTION ( 'NONE',  ( 1.000000000000000000, 0.000000000000000000, 0.000000000000000000 ) ) ;
#22047=DIRECTION ( 'NONE',  ( -1.000000000000000000, 0.000000000000000000, 0.000000000000000000 ) ) ;
#22115=DIRECTION ( 'NONE',  ( 0.000000000000000000, 0.000000000000000000, -1.000000000000000000 ) ) ;
#22118=EDGE_LOOP ( 'NONE', ( #14557, #1748 ) ) ;
#22151=CARTESIAN_POINT ( 'NONE',  ( 0.03008364706454716778, -0.2273032555864669124, 2.185478346456692557E-17 ) ) ;
#22375=DIRECTION ( 'NONE',  ( 0.5000000010362839475, 0.000000000000000000, 0.8660254031861397417 ) ) ;
#22387=EDGE_CURVE ( 'NONE', #26154, #3526, #15773, .T. ) ;
#22590=DIRECTION ( 'NONE',  ( -0.000000000000000000, 0.8660254037844388186, 0.4999999999999998890 ) ) ;
#22657=ORIENTED_EDGE ( 'NONE', *, *, #20245, .F. ) ;
#22890=PLANE ( 'NONE',  #633 ) ;
#22935=VECTOR ( 'NONE', #8663, 39.37007874015748143 ) ;
#22993=PLANE ( 'NONE',  #15465 ) ;
#23008=ADVANCED_FACE ( 'NONE', ( #20714 ), #1093, .T. ) ;
#23033=( BOUNDED_CURVE ( )  B_SPLINE_CURVE ( 2, ( #17623, #17355, #26239 ),
 .UNSPECIFIED., .F., .T. ) 
 B_SPLINE_CURVE_WITH_KNOTS ( ( 3, 3 ),
 ( 0.000000000000000000, 0.5842180690389598974 ),
 .UNSPECIFIED. ) 
 CURVE ( )  GEOMETRIC_REPRESENTATION_ITEM ( )  RATIONAL_B_SPLINE_CURVE ( ( 1.000000000000000000, 1.154700538379249908, 1.000000000000000000 ) ) 
 REPRESENTATION_ITEM ( '' )  ) ;
#23034=DIRECTION ( 'NONE',  ( 0.000000000000000000, -0.8660254037844384856, -0.5000000000000003331 ) ) ;
#23089=CARTESIAN_POINT ( 'NONE',  ( -0.4895985792973480133, 1.185352029804633059E-17, 0.09679133858267717494 ) ) ;
#23126=AXIS2_PLACEMENT_3D ( 'NONE', #25514, #16306, #9362 ) ;
#23203=ORIENTED_EDGE ( 'NONE', *, *, #13983, .F. ) ;
#23218=AXIS2_PLACEMENT_3D ( 'NONE', #7918, #5375, #11863 ) ;
#23241=ADVANCED_FACE ( 'NONE', ( #16904 ), #3237, .T. ) ;
#23242=CONICAL_SURFACE ( 'NONE', #11046, 0.1074461786882927178, 1.047197550000000144 ) ;
#23258=CARTESIAN_POINT ( 'NONE',  ( 0.000000000000000000, 0.1136516277932338587, -0.1968503937007874127 ) ) ;
#23283=ORIENTED_EDGE ( 'NONE', *, *, #10512, .F. ) ;
#23285=DIRECTION ( 'NONE',  ( 0.000000000000000000, 0.000000000000000000, 1.000000000000000000 ) ) ;
#23360=DIRECTION ( 'NONE',  ( 0.5000000010362839475, 0.8660254031861397417, 0.000000000000000000 ) ) ;
#23442=( CONVERSION_BASED_UNIT ( 'INCH', #15102 ) LENGTH_UNIT ( ) NAMED_UNIT ( #7220 ) ) ;
#23488=CARTESIAN_POINT ( 'NONE',  ( 0.03008364706454716778, 0.2273032555864669124, 9.010881889763779798E-17 ) ) ;
#23522=AXIS2_PLACEMENT_3D ( 'NONE', #24098, #13216, #22115 ) ;
#23540=FACE_OUTER_BOUND ( 'NONE', #16840, .T. ) ;
#23590=DIRECTION ( 'NONE',  ( 0.000000000000000000, 1.000000000000000000, 0.000000000000000000 ) ) ;
#23644=CARTESIAN_POINT ( 'NONE',  ( -0.002724751885584015491, -0.1704774416898501010, 0.09842519685039370636 ) ) ;
#23655=EDGE_CURVE ( 'NONE', #11206, #20886, #12377, .T. ) ;
#23671=ORIENTED_EDGE ( 'NONE', *, *, #16737, .F. ) ;
#23725=CARTESIAN_POINT ( 'NONE',  ( 0.1109424284362303254, 0.000000000000000000, 0.000000000000000000 ) ) ;
#23756=DIRECTION ( 'NONE',  ( 1.000000000000000000, 0.000000000000000000, 0.000000000000000000 ) ) ;
#23850=ADVANCED_BREP_SHAPE_REPRESENTATION ( 'M6 Thin Hex Nut', ( #3447, #11588 ), #15695 ) ;
#23925=FILL_AREA_STYLE ('',( #352 ) ) ;
#24078=CIRCLE ( 'NONE', #20040, 0.09679133858267717494 ) ;
#24084=EDGE_CURVE ( 'NONE', #9496, #25577, #18045, .T. ) ;
#24098=CARTESIAN_POINT ( 'NONE',  ( 0.000000000000000000, 0.000000000000000000, 0.000000000000000000 ) ) ;
#24123=AXIS2_PLACEMENT_3D ( 'NONE', #2063, #1505, #1653 ) ;
#24139=ORIENTED_EDGE ( 'NONE', *, *, #5317, .F. ) ;
#24149=ADVANCED_FACE ( 'NONE', ( #5939, #25136 ), #22890, .T. ) ;
#24166=EDGE_CURVE ( 'NONE', #13350, #12714, #20472, .T. ) ;
#24176=EDGE_CURVE ( 'NONE', #17596, #15474, #19052, .T. ) ;
#24182=CARTESIAN_POINT ( 'NONE',  ( 0.03008364706454716778, 0.2273032555864669124, 0.000000000000000000 ) ) ;
#24348=AXIS2_PLACEMENT_3D ( 'NONE', #15115, #13107, #12964 ) ;
#24359=EDGE_CURVE ( 'NONE', #657, #3526, #3145, .T. ) ;
#24416=CARTESIAN_POINT ( 'NONE',  ( 0.09590060490395689585, -0.1136516277932334562, 0.1968503937007874127 ) ) ;
#24509=VERTEX_POINT ( 'NONE', #5988 ) ;
#24525=EDGE_CURVE ( 'NONE', #3577, #15134, #18676, .T. ) ;
#24539=CARTESIAN_POINT ( 'NONE',  ( 0.03008364706454716778, -0.1136516277932324709, -0.1968503937007874127 ) ) ;
#24567=CARTESIAN_POINT ( 'NONE',  ( 0.1198326771653543399, -1.315836188112322458E-17, -0.1074461786882927178 ) ) ;
#24621=CARTESIAN_POINT ( 'NONE',  ( 0.03008364706454716778, 0.1136516277932340530, -0.1968503937007874127 ) ) ;
#24646=CARTESIAN_POINT ( 'NONE',  ( 0.09590060490395689585, 0.1136516277932334562, 0.1968503937007874127 ) ) ;
#24717=EDGE_CURVE ( 'NONE', #19119, #2155, #244, .T. ) ;
#24986=CARTESIAN_POINT ( 'NONE',  ( 0.1259842519685039353, 0.000000000000000000, 0.000000000000000000 ) ) ;
#24992=DIRECTION ( 'NONE',  ( 1.000000000000000000, 0.000000000000000000, 0.000000000000000000 ) ) ;
#25015=CARTESIAN_POINT ( 'NONE',  ( 0.1109424284362303254, -0.2012500529900838608, -2.464602332225414408E-17 ) ) ;
#25099=EDGE_LOOP ( 'NONE', ( #23283, #20769, #9876, #27797 ) ) ;
#25102=SURFACE_STYLE_FILL_AREA ( #23925 ) ;
#25136=FACE_OUTER_BOUND ( 'NONE', #21230, .T. ) ;
#25138=ADVANCED_FACE ( 'NONE', ( #6444 ), #9213, .F. ) ;
#25278=CARTESIAN_POINT ( 'NONE',  ( 0.1259842519685039353, 0.000000000000000000, 0.000000000000000000 ) ) ;
#25279=DIRECTION ( 'NONE',  ( 1.000000000000000000, 0.000000000000000000, 0.000000000000000000 ) ) ;
#25321=VECTOR ( 'NONE', #9032, 39.37007874015748854 ) ;
#25434=CONICAL_SURFACE ( 'NONE', #13685, 0.2012500529900838608, 1.047197550000000144 ) ;
#25455=CONICAL_SURFACE ( 'NONE', #8324, 0.1074461786882927178, 1.047197550000000144 ) ;
#25514=CARTESIAN_POINT ( 'NONE',  ( 0.01504182353227358389, 0.000000000000000000, 0.000000000000000000 ) ) ;
#25543=( NAMED_UNIT ( * ) SI_UNIT ( $, .STERADIAN. ) SOLID_ANGLE_UNIT ( ) ) ;
#25577=VERTEX_POINT ( 'NONE', #5396 ) ;
#25591=DIRECTION ( 'NONE',  ( -0.5000000010362839475, -0.8660254031861397417, -1.060575237992202059E-16 ) ) ;
#25609=CARTESIAN_POINT ( 'NONE',  ( 0.03008364706454716778, 0.1136516277932334562, 0.1968503937007874127 ) ) ;
#25634=EDGE_LOOP ( 'NONE', ( #13041, #27269, #8287, #12195 ) ) ;
#25970=FACE_OUTER_BOUND ( 'NONE', #9001, .T. ) ;
#26100=VERTEX_POINT ( 'NONE', #21770 ) ;
#26127=( BOUNDED_CURVE ( )  B_SPLINE_CURVE ( 2, ( #16427, #14468, #25609 ),
 .UNSPECIFIED., .F., .F. ) 
 B_SPLINE_CURVE_WITH_KNOTS ( ( 3, 3 ),
 ( 0.000000000000000000, 0.5842180690389588982 ),
 .UNSPECIFIED. ) 
 CURVE ( )  GEOMETRIC_REPRESENTATION_ITEM ( )  RATIONAL_B_SPLINE_CURVE ( ( 1.000000000000000000, 1.154700538379251906, 1.000000000000000000 ) ) 
 REPRESENTATION_ITEM ( '' )  ) ;
#26154=VERTEX_POINT ( 'NONE', #19918 ) ;
#26239=CARTESIAN_POINT ( 'NONE',  ( 0.09590060490395689585, -0.2273032555864669124, 2.185478346456692557E-17 ) ) ;
#26246=CARTESIAN_POINT ( 'NONE',  ( 0.1109424284362303254, 0.000000000000000000, 0.000000000000000000 ) ) ;
#26333=VECTOR ( 'NONE', #5219, 39.37007874015748143 ) ;
#26359=EDGE_LOOP ( 'NONE', ( #7462, #5975, #3023, #10707, #24139, #19349 ) ) ;
#26388=DIRECTION ( 'NONE',  ( -0.5000000010362839475, 0.000000000000000000, -0.8660254031861397417 ) ) ;
#26471=ADVANCED_FACE ( 'NONE', ( #13157 ), #7213, .F. ) ;
#26535=CARTESIAN_POINT ( 'NONE',  ( 0.000000000000000000, 4.370956692913385731E-17, -8.195543307086614694E-17 ) ) ;
#26631=ORIENTED_EDGE ( 'NONE', *, *, #8001, .F. ) ;
#26817=ORIENTED_EDGE ( 'NONE', *, *, #19240, .T. ) ;
#26966=ORIENTED_EDGE ( 'NONE', *, *, #14413, .F. ) ;
#26971=ORIENTED_EDGE ( 'NONE', *, *, #14413, .T. ) ;
#27043=CARTESIAN_POINT ( 'NONE',  ( 0.1198326771653543399, 0.000000000000000000, 0.1074461786882927178 ) ) ;
#27063=AXIS2_PLACEMENT_3D ( 'NONE', #19773, #6789, #15423 ) ;
#27129=DIRECTION ( 'NONE',  ( 0.000000000000000000, 1.000000000000000000, 0.000000000000000000 ) ) ;
#27234=DIRECTION ( 'NONE',  ( 0.000000000000000000, 0.000000000000000000, 1.000000000000000000 ) ) ;
#27269=ORIENTED_EDGE ( 'NONE', *, *, #13804, .T. ) ;
#27311=DIRECTION ( 'NONE',  ( -1.000000000000000000, 0.000000000000000000, 0.000000000000000000 ) ) ;
#27346=CARTESIAN_POINT ( 'NONE',  ( 0.1287090038540880110, 0.000000000000000000, 0.1968503937007874127 ) ) ;
#27370=CARTESIAN_POINT ( 'NONE',  ( 0.1136811023622047168, 0.000000000000000000, 0.000000000000000000 ) ) ;
#27376=CARTESIAN_POINT ( 'NONE',  ( 0.1259842519685039353, 0.000000000000000000, 0.000000000000000000 ) ) ;
#27386=SHAPE_REPRESENTATION_RELATIONSHIP ( 'NONE' , 'NONE' ,  #16232, #23850 ) ;
#27467=ORIENTED_EDGE ( 'NONE', *, *, #20014, .T. ) ;
#27515=EDGE_CURVE ( 'NONE', #12714, #26100, #13897, .T. ) ;
#27552=DIRECTION ( 'NONE',  ( 0.000000000000000000, 0.000000000000000000, -1.000000000000000000 ) ) ;
#27568=ORIENTED_EDGE ( 'NONE', *, *, #4796, .F. ) ;
#27618=EDGE_CURVE ( 'NONE', #657, #26100, #9293, .T. ) ;
#27729=AXIS2_PLACEMENT_3D ( 'NONE', #12050, #27311, #21236 ) ;
#27797=ORIENTED_EDGE ( 'NONE', *, *, #12242, .T. ) ;
#27809=DIRECTION ( 'NONE',  ( -0.5000000010362839475, -1.060575237992202059E-16, 0.8660254031861397417 ) ) ;
ENDSEC;
END-ISO-10303-21;
